ISO-10303-21;
HEADER;
/* Generated by software containing ST-Developer
 * from STEP Tools, Inc. (www.steptools.com) 
 */

FILE_DESCRIPTION(
/* description */ ('Double-row support with tensioned shaft'),
/* implementation_level */ '2;1');

FILE_NAME(
/* name */ 'Socket Set Screw - M5x8.step',
/* time_stamp */ '2026-10-27T10:50:35-07:00',
/* author */ (''),
/* organization */ (''),
/* preprocessor_version */ 'ST-DEVELOPER v20.2',
/* originating_system */ 'Autodesk Translation Framework v15.17.0.0',
/* authorisation */ '');

FILE_SCHEMA (('AUTOMOTIVE_DESIGN { 1 0 10303 214 3 1 1 }'));
ENDSEC;

DATA;
#10=MECHANICAL_DESIGN_GEOMETRIC_PRESENTATION_REPRESENTATION('',(#511),#11559);
#405=CONICAL_SURFACE('',#7354,0.235,0.785398163397448);
#406=CONICAL_SURFACE('',#7358,0.2125,0.785398163397448);
#446=SHAPE_REPRESENTATION_RELATIONSHIP('SRR','None',#11756,#478);
#478=ADVANCED_BREP_SHAPE_REPRESENTATION('',(#541),#11558);
#511=STYLED_ITEM('',(#11974),#541);
#541=MANIFOLD_SOLID_BREP('Body1',#6359);
#678=FACE_BOUND('',#1737,.T.);
#908=PLANE('',#7345);
#909=PLANE('',#7346);
#910=PLANE('',#7347);
#911=PLANE('',#7348);
#912=PLANE('',#7349);
#913=PLANE('',#7350);
#914=PLANE('',#7351);
#915=PLANE('',#7352);
#916=PLANE('',#7360);
#1249=FACE_OUTER_BOUND('',#1729,.T.);
#1250=FACE_OUTER_BOUND('',#1730,.T.);
#1251=FACE_OUTER_BOUND('',#1731,.T.);
#1252=FACE_OUTER_BOUND('',#1732,.T.);
#1253=FACE_OUTER_BOUND('',#1733,.T.);
#1254=FACE_OUTER_BOUND('',#1734,.T.);
#1255=FACE_OUTER_BOUND('',#1735,.T.);
#1256=FACE_OUTER_BOUND('',#1736,.T.);
#1257=FACE_OUTER_BOUND('',#1738,.T.);
#1258=FACE_OUTER_BOUND('',#1739,.T.);
#1259=FACE_OUTER_BOUND('',#1740,.T.);
#1260=FACE_OUTER_BOUND('',#1741,.T.);
#1729=EDGE_LOOP('',(#5840,#5841,#5842,#5843));
#1730=EDGE_LOOP('',(#5844,#5845,#5846,#5847));
#1731=EDGE_LOOP('',(#5848,#5849,#5850,#5851));
#1732=EDGE_LOOP('',(#5852,#5853,#5854,#5855));
#1733=EDGE_LOOP('',(#5856,#5857,#5858,#5859));
#1734=EDGE_LOOP('',(#5860,#5861,#5862,#5863));
#1735=EDGE_LOOP('',(#5864,#5865,#5866,#5867,#5868,#5869));
#1736=EDGE_LOOP('',(#5870));
#1737=EDGE_LOOP('',(#5871,#5872,#5873,#5874,#5875,#5876));
#1738=EDGE_LOOP('',(#5877,#5878,#5879,#5880));
#1739=EDGE_LOOP('',(#5881,#5882,#5883,#5884));
#1740=EDGE_LOOP('',(#5885,#5886,#5887,#5888));
#1741=EDGE_LOOP('',(#5889));
#2268=LINE('',#11426,#2815);
#2269=LINE('',#11428,#2816);
#2270=LINE('',#11430,#2817);
#2271=LINE('',#11431,#2818);
#2272=LINE('',#11434,#2819);
#2273=LINE('',#11436,#2820);
#2274=LINE('',#11437,#2821);
#2275=LINE('',#11440,#2822);
#2276=LINE('',#11442,#2823);
#2277=LINE('',#11443,#2824);
#2278=LINE('',#11446,#2825);
#2279=LINE('',#11448,#2826);
#2280=LINE('',#11449,#2827);
#2281=LINE('',#11452,#2828);
#2282=LINE('',#11454,#2829);
#2283=LINE('',#11455,#2830);
#2284=LINE('',#11457,#2831);
#2285=LINE('',#11458,#2832);
#2286=LINE('',#11466,#2833);
#2287=LINE('',#11470,#2834);
#2288=LINE('',#11474,#2835);
#2815=VECTOR('',#9163,1.);
#2816=VECTOR('',#9164,1.);
#2817=VECTOR('',#9165,1.);
#2818=VECTOR('',#9166,1.);
#2819=VECTOR('',#9169,1.);
#2820=VECTOR('',#9170,1.);
#2821=VECTOR('',#9171,1.);
#2822=VECTOR('',#9174,1.);
#2823=VECTOR('',#9175,1.);
#2824=VECTOR('',#9176,1.);
#2825=VECTOR('',#9179,1.);
#2826=VECTOR('',#9180,1.);
#2827=VECTOR('',#9181,1.);
#2828=VECTOR('',#9184,1.);
#2829=VECTOR('',#9185,1.);
#2830=VECTOR('',#9186,1.);
#2831=VECTOR('',#9189,1.);
#2832=VECTOR('',#9190,1.);
#2833=VECTOR('',#9201,0.235);
#2834=VECTOR('',#9206,0.25);
#2835=VECTOR('',#9211,0.2125);
#3023=CIRCLE('',#7353,0.22);
#3024=CIRCLE('',#7355,0.24505);
#3025=CIRCLE('',#7357,0.24505);
#3026=CIRCLE('',#7359,0.175);
#3534=VERTEX_POINT('',#11424);
#3535=VERTEX_POINT('',#11425);
#3536=VERTEX_POINT('',#11427);
#3537=VERTEX_POINT('',#11429);
#3538=VERTEX_POINT('',#11433);
#3539=VERTEX_POINT('',#11435);
#3540=VERTEX_POINT('',#11439);
#3541=VERTEX_POINT('',#11441);
#3542=VERTEX_POINT('',#11445);
#3543=VERTEX_POINT('',#11447);
#3544=VERTEX_POINT('',#11451);
#3545=VERTEX_POINT('',#11453);
#3546=VERTEX_POINT('',#11461);
#3547=VERTEX_POINT('',#11464);
#3548=VERTEX_POINT('',#11468);
#3549=VERTEX_POINT('',#11472);
#4305=EDGE_CURVE('',#3534,#3535,#2268,.T.);
#4306=EDGE_CURVE('',#3534,#3536,#2269,.T.);
#4307=EDGE_CURVE('',#3536,#3537,#2270,.T.);
#4308=EDGE_CURVE('',#3535,#3537,#2271,.T.);
#4309=EDGE_CURVE('',#3538,#3534,#2272,.T.);
#4310=EDGE_CURVE('',#3538,#3539,#2273,.T.);
#4311=EDGE_CURVE('',#3539,#3536,#2274,.T.);
#4312=EDGE_CURVE('',#3540,#3538,#2275,.T.);
#4313=EDGE_CURVE('',#3540,#3541,#2276,.T.);
#4314=EDGE_CURVE('',#3541,#3539,#2277,.T.);
#4315=EDGE_CURVE('',#3542,#3540,#2278,.T.);
#4316=EDGE_CURVE('',#3542,#3543,#2279,.T.);
#4317=EDGE_CURVE('',#3543,#3541,#2280,.T.);
#4318=EDGE_CURVE('',#3544,#3542,#2281,.T.);
#4319=EDGE_CURVE('',#3544,#3545,#2282,.T.);
#4320=EDGE_CURVE('',#3545,#3543,#2283,.T.);
#4321=EDGE_CURVE('',#3535,#3544,#2284,.T.);
#4322=EDGE_CURVE('',#3537,#3545,#2285,.T.);
#4323=EDGE_CURVE('',#3546,#3546,#3023,.T.);
#4324=EDGE_CURVE('',#3547,#3547,#3024,.T.);
#4325=EDGE_CURVE('',#3547,#3546,#2286,.T.);
#4326=EDGE_CURVE('',#3548,#3548,#3025,.F.);
#4327=EDGE_CURVE('',#3548,#3547,#2287,.T.);
#4328=EDGE_CURVE('',#3549,#3549,#3026,.T.);
#4329=EDGE_CURVE('',#3549,#3548,#2288,.T.);
#5840=ORIENTED_EDGE('',*,*,#4305,.F.);
#5841=ORIENTED_EDGE('',*,*,#4306,.T.);
#5842=ORIENTED_EDGE('',*,*,#4307,.T.);
#5843=ORIENTED_EDGE('',*,*,#4308,.F.);
#5844=ORIENTED_EDGE('',*,*,#4309,.F.);
#5845=ORIENTED_EDGE('',*,*,#4310,.T.);
#5846=ORIENTED_EDGE('',*,*,#4311,.T.);
#5847=ORIENTED_EDGE('',*,*,#4306,.F.);
#5848=ORIENTED_EDGE('',*,*,#4312,.F.);
#5849=ORIENTED_EDGE('',*,*,#4313,.T.);
#5850=ORIENTED_EDGE('',*,*,#4314,.T.);
#5851=ORIENTED_EDGE('',*,*,#4310,.F.);
#5852=ORIENTED_EDGE('',*,*,#4315,.F.);
#5853=ORIENTED_EDGE('',*,*,#4316,.T.);
#5854=ORIENTED_EDGE('',*,*,#4317,.T.);
#5855=ORIENTED_EDGE('',*,*,#4313,.F.);
#5856=ORIENTED_EDGE('',*,*,#4318,.F.);
#5857=ORIENTED_EDGE('',*,*,#4319,.T.);
#5858=ORIENTED_EDGE('',*,*,#4320,.T.);
#5859=ORIENTED_EDGE('',*,*,#4316,.F.);
#5860=ORIENTED_EDGE('',*,*,#4321,.F.);
#5861=ORIENTED_EDGE('',*,*,#4308,.T.);
#5862=ORIENTED_EDGE('',*,*,#4322,.T.);
#5863=ORIENTED_EDGE('',*,*,#4319,.F.);
#5864=ORIENTED_EDGE('',*,*,#4322,.F.);
#5865=ORIENTED_EDGE('',*,*,#4307,.F.);
#5866=ORIENTED_EDGE('',*,*,#4311,.F.);
#5867=ORIENTED_EDGE('',*,*,#4314,.F.);
#5868=ORIENTED_EDGE('',*,*,#4317,.F.);
#5869=ORIENTED_EDGE('',*,*,#4320,.F.);
#5870=ORIENTED_EDGE('',*,*,#4323,.F.);
#5871=ORIENTED_EDGE('',*,*,#4305,.T.);
#5872=ORIENTED_EDGE('',*,*,#4321,.T.);
#5873=ORIENTED_EDGE('',*,*,#4318,.T.);
#5874=ORIENTED_EDGE('',*,*,#4315,.T.);
#5875=ORIENTED_EDGE('',*,*,#4312,.T.);
#5876=ORIENTED_EDGE('',*,*,#4309,.T.);
#5877=ORIENTED_EDGE('',*,*,#4324,.F.);
#5878=ORIENTED_EDGE('',*,*,#4325,.T.);
#5879=ORIENTED_EDGE('',*,*,#4323,.T.);
#5880=ORIENTED_EDGE('',*,*,#4325,.F.);
#5881=ORIENTED_EDGE('',*,*,#4326,.F.);
#5882=ORIENTED_EDGE('',*,*,#4327,.T.);
#5883=ORIENTED_EDGE('',*,*,#4324,.T.);
#5884=ORIENTED_EDGE('',*,*,#4327,.F.);
#5885=ORIENTED_EDGE('',*,*,#4328,.F.);
#5886=ORIENTED_EDGE('',*,*,#4329,.T.);
#5887=ORIENTED_EDGE('',*,*,#4326,.T.);
#5888=ORIENTED_EDGE('',*,*,#4329,.F.);
#5889=ORIENTED_EDGE('',*,*,#4328,.T.);
#5979=CYLINDRICAL_SURFACE('',#7356,0.24505);
#6312=ADVANCED_FACE('',(#1249),#908,.F.);
#6313=ADVANCED_FACE('',(#1250),#909,.F.);
#6314=ADVANCED_FACE('',(#1251),#910,.F.);
#6315=ADVANCED_FACE('',(#1252),#911,.F.);
#6316=ADVANCED_FACE('',(#1253),#912,.F.);
#6317=ADVANCED_FACE('',(#1254),#913,.F.);
#6318=ADVANCED_FACE('',(#1255),#914,.F.);
#6319=ADVANCED_FACE('',(#1256,#678),#915,.T.);
#6320=ADVANCED_FACE('',(#1257),#405,.T.);
#6321=ADVANCED_FACE('',(#1258),#5979,.T.);
#6322=ADVANCED_FACE('',(#1259),#406,.T.);
#6323=ADVANCED_FACE('',(#1260),#916,.T.);
#6359=CLOSED_SHELL('',(#6312,#6313,#6314,#6315,#6316,#6317,#6318,#6319,
#6320,#6321,#6322,#6323));
#7344=AXIS2_PLACEMENT_3D('',#11422,#9159,#9160);
#7345=AXIS2_PLACEMENT_3D('',#11423,#9161,#9162);
#7346=AXIS2_PLACEMENT_3D('',#11432,#9167,#9168);
#7347=AXIS2_PLACEMENT_3D('',#11438,#9172,#9173);
#7348=AXIS2_PLACEMENT_3D('',#11444,#9177,#9178);
#7349=AXIS2_PLACEMENT_3D('',#11450,#9182,#9183);
#7350=AXIS2_PLACEMENT_3D('',#11456,#9187,#9188);
#7351=AXIS2_PLACEMENT_3D('',#11459,#9191,#9192);
#7352=AXIS2_PLACEMENT_3D('',#11460,#9193,#9194);
#7353=AXIS2_PLACEMENT_3D('',#11462,#9195,#9196);
#7354=AXIS2_PLACEMENT_3D('',#11463,#9197,#9198);
#7355=AXIS2_PLACEMENT_3D('',#11465,#9199,#9200);
#7356=AXIS2_PLACEMENT_3D('',#11467,#9202,#9203);
#7357=AXIS2_PLACEMENT_3D('',#11469,#9204,#9205);
#7358=AXIS2_PLACEMENT_3D('',#11471,#9207,#9208);
#7359=AXIS2_PLACEMENT_3D('',#11473,#9209,#9210);
#7360=AXIS2_PLACEMENT_3D('',#11475,#9212,#9213);
#9159=DIRECTION('axis',(0.,0.,1.));
#9160=DIRECTION('refdir',(1.,0.,0.));
#9161=DIRECTION('center_axis',(0.866025403784439,0.,-0.5));
#9162=DIRECTION('ref_axis',(0.5,0.,0.866025403784439));
#9163=DIRECTION('',(0.5,0.,0.866025403784439));
#9164=DIRECTION('',(0.,-1.,0.));
#9165=DIRECTION('',(0.5,0.,0.866025403784439));
#9166=DIRECTION('',(0.,-1.,0.));
#9167=DIRECTION('center_axis',(1.92296268638356E-16,0.,-1.));
#9168=DIRECTION('ref_axis',(1.,0.,1.92296268638356E-16));
#9169=DIRECTION('',(1.,0.,1.92296268638356E-16));
#9170=DIRECTION('',(0.,-1.,0.));
#9171=DIRECTION('',(1.,0.,1.92296268638356E-16));
#9172=DIRECTION('center_axis',(-0.866025403784439,0.,-0.5));
#9173=DIRECTION('ref_axis',(0.5,0.,-0.866025403784439));
#9174=DIRECTION('',(0.5,0.,-0.866025403784439));
#9175=DIRECTION('',(0.,-1.,0.));
#9176=DIRECTION('',(0.5,0.,-0.866025403784438));
#9177=DIRECTION('center_axis',(-0.866025403784439,0.,0.5));
#9178=DIRECTION('ref_axis',(-0.5,0.,-0.866025403784439));
#9179=DIRECTION('',(-0.5,0.,-0.866025403784439));
#9180=DIRECTION('',(0.,-1.,0.));
#9181=DIRECTION('',(-0.5,0.,-0.866025403784439));
#9182=DIRECTION('center_axis',(-1.92296268638356E-16,0.,1.));
#9183=DIRECTION('ref_axis',(-1.,0.,-1.92296268638356E-16));
#9184=DIRECTION('',(-1.,0.,-1.92296268638356E-16));
#9185=DIRECTION('',(0.,-1.,0.));
#9186=DIRECTION('',(-1.,0.,-1.92296268638356E-16));
#9187=DIRECTION('center_axis',(0.866025403784439,0.,0.5));
#9188=DIRECTION('ref_axis',(-0.5,0.,0.866025403784439));
#9189=DIRECTION('',(-0.5,0.,0.866025403784439));
#9190=DIRECTION('',(-0.5,0.,0.866025403784439));
#9191=DIRECTION('center_axis',(0.,-1.,0.));
#9192=DIRECTION('ref_axis',(0.,0.,-1.));
#9193=DIRECTION('center_axis',(0.,1.,0.));
#9194=DIRECTION('ref_axis',(0.,0.,1.));
#9195=DIRECTION('center_axis',(0.,-1.,0.));
#9196=DIRECTION('ref_axis',(1.,0.,0.));
#9197=DIRECTION('center_axis',(0.,-1.,0.));
#9198=DIRECTION('ref_axis',(1.,0.,0.));
#9199=DIRECTION('center_axis',(0.,-1.,0.));
#9200=DIRECTION('ref_axis',(1.,0.,0.));
#9201=DIRECTION('',(0.707106781186547,0.707106781186548,8.65956056235493E-17));
#9202=DIRECTION('center_axis',(0.,-1.,0.));
#9203=DIRECTION('ref_axis',(1.,0.,0.));
#9204=DIRECTION('center_axis',(0.,1.,0.));
#9205=DIRECTION('ref_axis',(1.,0.,0.));
#9206=DIRECTION('',(0.,1.,0.));
#9207=DIRECTION('center_axis',(0.,1.,0.));
#9208=DIRECTION('ref_axis',(1.,0.,0.));
#9209=DIRECTION('center_axis',(0.,-1.,0.));
#9210=DIRECTION('ref_axis',(1.,0.,0.));
#9211=DIRECTION('',(-0.707106781186547,0.707106781186548,-8.65956056235493E-17));
#9212=DIRECTION('center_axis',(0.,-1.,0.));
#9213=DIRECTION('ref_axis',(0.,0.,-1.));
#11422=CARTESIAN_POINT('',(0.,0.,0.));
#11423=CARTESIAN_POINT('Origin',(0.0721687836487032,0.,-0.125));
#11424=CARTESIAN_POINT('',(0.0721687836487032,0.,-0.125));
#11425=CARTESIAN_POINT('',(0.144337567297406,0.,0.));
#11426=CARTESIAN_POINT('',(0.117710979560879,0.,-0.0461186027918559));
#11427=CARTESIAN_POINT('',(0.0721687836487032,-0.25,-0.125));
#11428=CARTESIAN_POINT('',(0.0721687836487032,0.,-0.125));
#11429=CARTESIAN_POINT('',(0.144337567297406,-0.25,0.));
#11430=CARTESIAN_POINT('',(0.144337567297406,-0.25,0.));
#11431=CARTESIAN_POINT('',(0.144337567297406,0.,0.));
#11432=CARTESIAN_POINT('Origin',(-0.0721687836487032,0.,-0.125));
#11433=CARTESIAN_POINT('',(-0.0721687836487032,0.,-0.125));
#11434=CARTESIAN_POINT('',(0.0739156081756484,0.,-0.125));
#11435=CARTESIAN_POINT('',(-0.0721687836487032,-0.25,-0.125));
#11436=CARTESIAN_POINT('',(-0.0721687836487032,0.,-0.125));
#11437=CARTESIAN_POINT('',(0.0721687836487032,-0.25,-0.125));
#11438=CARTESIAN_POINT('Origin',(-0.144337567297406,0.,-4.16333634234434E-17));
#11439=CARTESIAN_POINT('',(-0.144337567297406,0.,-1.76762539787485E-17));
#11440=CARTESIAN_POINT('',(-0.0987953713852306,0.,-0.0788813972081442));
#11441=CARTESIAN_POINT('',(-0.144337567297406,-0.25,-2.77555756156289E-17));
#11442=CARTESIAN_POINT('',(-0.144337567297406,0.,-1.76762539787485E-17));
#11443=CARTESIAN_POINT('',(-0.0721687836487032,-0.25,-0.125));
#11444=CARTESIAN_POINT('Origin',(-0.0721687836487033,0.,0.125));
#11445=CARTESIAN_POINT('',(-0.0721687836487033,0.,0.125));
#11446=CARTESIAN_POINT('',(-0.0627109795608791,0.,0.141381397208144));
#11447=CARTESIAN_POINT('',(-0.0721687836487033,-0.25,0.125));
#11448=CARTESIAN_POINT('',(-0.0721687836487033,0.,0.125));
#11449=CARTESIAN_POINT('',(-0.144337567297406,-0.25,-1.76762539787485E-17));
#11450=CARTESIAN_POINT('Origin',(0.0721687836487032,0.,0.125));
#11451=CARTESIAN_POINT('',(0.0721687836487032,0.,0.125));
#11452=CARTESIAN_POINT('',(0.146084391824352,0.,0.125));
#11453=CARTESIAN_POINT('',(0.0721687836487032,-0.25,0.125));
#11454=CARTESIAN_POINT('',(0.0721687836487032,0.,0.125));
#11455=CARTESIAN_POINT('',(-0.0721687836487033,-0.25,0.125));
#11456=CARTESIAN_POINT('Origin',(0.144337567297406,0.,0.));
#11457=CARTESIAN_POINT('',(0.153795371385231,0.,-0.0163813972081441));
#11458=CARTESIAN_POINT('',(0.0721687836487032,-0.25,0.125));
#11459=CARTESIAN_POINT('Origin',(0.,-0.25,0.));
#11460=CARTESIAN_POINT('Origin',(0.22,0.,0.));
#11461=CARTESIAN_POINT('',(-0.22,-8.67361737988404E-18,-2.69422295812418E-17));
#11462=CARTESIAN_POINT('Origin',(0.,0.,0.));
#11463=CARTESIAN_POINT('Origin',(0.,-0.015,0.));
#11464=CARTESIAN_POINT('',(-0.24505,-0.02505,-3.00099698131059E-17));
#11465=CARTESIAN_POINT('Origin',(0.,-0.02505,0.));
#11466=CARTESIAN_POINT('',(-0.235,-0.015,-2.87791997799628E-17));
#11467=CARTESIAN_POINT('Origin',(0.,-0.3775,0.));
#11468=CARTESIAN_POINT('',(-0.24505,-0.72995,3.00099698131059E-17));
#11469=CARTESIAN_POINT('Origin',(0.,-0.72995,0.));
#11470=CARTESIAN_POINT('',(-0.24505,-0.3775,-3.00099698131059E-17));
#11471=CARTESIAN_POINT('Origin',(0.,-0.7625,0.));
#11472=CARTESIAN_POINT('',(-0.175,-0.8,-2.14313189850787E-17));
#11473=CARTESIAN_POINT('Origin',(0.,-0.8,0.));
#11474=CARTESIAN_POINT('',(-0.2125,-0.7625,-2.60237444818813E-17));
#11475=CARTESIAN_POINT('Origin',(0.,-0.8,0.));
#11521=UNCERTAINTY_MEASURE_WITH_UNIT(LENGTH_MEASURE(0.001),#11560,
'DISTANCE_ACCURACY_VALUE',
'Maximum model space distance between geometric entities at asserted c
onnectivities');
#11522=UNCERTAINTY_MEASURE_WITH_UNIT(LENGTH_MEASURE(0.001),#11560,
'DISTANCE_ACCURACY_VALUE',
'Maximum model space distance between geometric entities at asserted c
onnectivities');
#11558=(
GEOMETRIC_REPRESENTATION_CONTEXT(3)
GLOBAL_UNCERTAINTY_ASSIGNED_CONTEXT((#11521))
GLOBAL_UNIT_ASSIGNED_CONTEXT((#11560,#11562,#11563))
REPRESENTATION_CONTEXT('','3D')
);
#11559=(
GEOMETRIC_REPRESENTATION_CONTEXT(3)
GLOBAL_UNCERTAINTY_ASSIGNED_CONTEXT((#11522))
GLOBAL_UNIT_ASSIGNED_CONTEXT((#11560,#11562,#11563))
REPRESENTATION_CONTEXT('','3D')
);
#11560=(
LENGTH_UNIT()
NAMED_UNIT(*)
SI_UNIT(.CENTI.,.METRE.)
);
#11562=(
NAMED_UNIT(*)
PLANE_ANGLE_UNIT()
SI_UNIT($,.RADIAN.)
);
#11563=(
NAMED_UNIT(*)
SI_UNIT($,.STERADIAN.)
SOLID_ANGLE_UNIT()
);
#11599=SHAPE_DEFINITION_REPRESENTATION(#11710,#11756);
#11710=PRODUCT_DEFINITION_SHAPE('',$,#11793);
#11756=SHAPE_REPRESENTATION('',(#7344),#11558);
#11757=PRODUCT_DEFINITION_CONTEXT('part definition',#11867,'design');
#11793=PRODUCT_DEFINITION('Socket Set Screw - M5x8',
'Socket Set Screw - M5x8',#11829,#11757);
#11829=PRODUCT_DEFINITION_FORMATION('',$,#11904);
#11867=APPLICATION_CONTEXT(
'Core Data for Automotive Mechanical Design Process');
#11868=PRODUCT_CONTEXT('part definition',#11867,'mechanical');
#11904=PRODUCT('Socket Set Screw - M5x8','Socket Set Screw - M5x8',
'Socket Set Screw - M5x8',(#11868));
#11968=COLOUR_RGB('Black',0.12,0.14,0.17);
#11969=FILL_AREA_STYLE_COLOUR('',#11968);
#11970=FILL_AREA_STYLE('',(#11969));
#11971=SURFACE_STYLE_FILL_AREA(#11970);
#11972=SURFACE_SIDE_STYLE('',(#11971));
#11973=SURFACE_STYLE_USAGE(.BOTH.,#11972);
#11974=PRESENTATION_STYLE_ASSIGNMENT((#11973));
ENDSEC;
END-ISO-10303-21;
